ISO-10303-21;
HEADER;
/* Generated by software containing ST-Developer
 * from STEP Tools, Inc. (www.steptools.com) 
 */

FILE_DESCRIPTION(
/* description */ ('PAT-015'),
/* implementation_level */ '2;1');

FILE_NAME(
/* name */ 'Valve seat.step',
/* time_stamp */ '2026-10-29T16:03:43-07:00',
/* author */ (''),
/* organization */ (''),
/* preprocessor_version */ 'ST-DEVELOPER v20.2',
/* originating_system */ 'Autodesk Translation Framework v15.17.0.0',
/* authorisation */ '');

FILE_SCHEMA (('AUTOMOTIVE_DESIGN { 1 0 10303 214 3 1 1 }'));
ENDSEC;

DATA;
#10=MECHANICAL_DESIGN_GEOMETRIC_PRESENTATION_REPRESENTATION('',(#238),#10266);
#190=SHAPE_REPRESENTATION_RELATIONSHIP('SRR','None',#10361,#213);
#213=ADVANCED_BREP_SHAPE_REPRESENTATION('',(#263),#10249);
#238=STYLED_ITEM('',(#10561),#263);
#263=MANIFOLD_SOLID_BREP('Body1',#4697);
#364=FACE_BOUND('',#1062,.T.);
#365=FACE_BOUND('',#1064,.T.);
#487=PLANE('',#5229);
#488=PLANE('',#5230);
#704=FACE_OUTER_BOUND('',#1059,.T.);
#705=FACE_OUTER_BOUND('',#1060,.T.);
#706=FACE_OUTER_BOUND('',#1061,.T.);
#707=FACE_OUTER_BOUND('',#1063,.T.);
#1059=EDGE_LOOP('',(#3705,#3706,#3707,#3708));
#1060=EDGE_LOOP('',(#3709,#3710,#3711,#3712));
#1061=EDGE_LOOP('',(#3713));
#1062=EDGE_LOOP('',(#3714));
#1063=EDGE_LOOP('',(#3715));
#1064=EDGE_LOOP('',(#3716));
#1459=LINE('',#8682,#1739);
#1460=LINE('',#8688,#1740);
#1739=VECTOR('',#6202,0.2);
#1740=VECTOR('',#6209,0.6);
#1981=CIRCLE('',#5224,0.2);
#1982=CIRCLE('',#5225,0.2);
#1983=CIRCLE('',#5227,0.6);
#1984=CIRCLE('',#5228,0.6);
#2315=VERTEX_POINT('',#8679);
#2316=VERTEX_POINT('',#8681);
#2317=VERTEX_POINT('',#8685);
#2318=VERTEX_POINT('',#8687);
#2808=EDGE_CURVE('',#2315,#2315,#1981,.T.);
#2809=EDGE_CURVE('',#2315,#2316,#1459,.T.);
#2810=EDGE_CURVE('',#2316,#2316,#1982,.T.);
#2811=EDGE_CURVE('',#2317,#2317,#1983,.T.);
#2812=EDGE_CURVE('',#2317,#2318,#1460,.T.);
#2813=EDGE_CURVE('',#2318,#2318,#1984,.T.);
#3705=ORIENTED_EDGE('',*,*,#2808,.F.);
#3706=ORIENTED_EDGE('',*,*,#2809,.T.);
#3707=ORIENTED_EDGE('',*,*,#2810,.T.);
#3708=ORIENTED_EDGE('',*,*,#2809,.F.);
#3709=ORIENTED_EDGE('',*,*,#2811,.F.);
#3710=ORIENTED_EDGE('',*,*,#2812,.T.);
#3711=ORIENTED_EDGE('',*,*,#2813,.T.);
#3712=ORIENTED_EDGE('',*,*,#2812,.F.);
#3713=ORIENTED_EDGE('',*,*,#2811,.T.);
#3714=ORIENTED_EDGE('',*,*,#2808,.T.);
#3715=ORIENTED_EDGE('',*,*,#2813,.F.);
#3716=ORIENTED_EDGE('',*,*,#2810,.F.);
#4354=CYLINDRICAL_SURFACE('',#5223,0.2);
#4355=CYLINDRICAL_SURFACE('',#5226,0.6);
#4539=ADVANCED_FACE('',(#704),#4354,.F.);
#4540=ADVANCED_FACE('',(#705),#4355,.T.);
#4541=ADVANCED_FACE('',(#706,#364),#487,.T.);
#4542=ADVANCED_FACE('',(#707,#365),#488,.F.);
#4697=CLOSED_SHELL('',(#4539,#4540,#4541,#4542));
#5222=AXIS2_PLACEMENT_3D('',#8677,#6196,#6197);
#5223=AXIS2_PLACEMENT_3D('',#8678,#6198,#6199);
#5224=AXIS2_PLACEMENT_3D('',#8680,#6200,#6201);
#5225=AXIS2_PLACEMENT_3D('',#8683,#6203,#6204);
#5226=AXIS2_PLACEMENT_3D('',#8684,#6205,#6206);
#5227=AXIS2_PLACEMENT_3D('',#8686,#6207,#6208);
#5228=AXIS2_PLACEMENT_3D('',#8689,#6210,#6211);
#5229=AXIS2_PLACEMENT_3D('',#8690,#6212,#6213);
#5230=AXIS2_PLACEMENT_3D('',#8691,#6214,#6215);
#6196=DIRECTION('axis',(0.,0.,1.));
#6197=DIRECTION('refdir',(1.,0.,0.));
#6198=DIRECTION('center_axis',(0.,0.,1.));
#6199=DIRECTION('ref_axis',(1.,0.,0.));
#6200=DIRECTION('center_axis',(0.,0.,-1.));
#6201=DIRECTION('ref_axis',(1.,0.,0.));
#6202=DIRECTION('',(0.,0.,-1.));
#6203=DIRECTION('center_axis',(0.,0.,-1.));
#6204=DIRECTION('ref_axis',(1.,0.,0.));
#6205=DIRECTION('center_axis',(0.,0.,1.));
#6206=DIRECTION('ref_axis',(1.,0.,0.));
#6207=DIRECTION('center_axis',(0.,0.,1.));
#6208=DIRECTION('ref_axis',(1.,0.,0.));
#6209=DIRECTION('',(0.,0.,-1.));
#6210=DIRECTION('center_axis',(0.,0.,1.));
#6211=DIRECTION('ref_axis',(1.,0.,0.));
#6212=DIRECTION('center_axis',(0.,0.,1.));
#6213=DIRECTION('ref_axis',(1.,0.,0.));
#6214=DIRECTION('center_axis',(0.,0.,1.));
#6215=DIRECTION('ref_axis',(1.,0.,0.));
#8677=CARTESIAN_POINT('',(0.,0.,0.));
#8678=CARTESIAN_POINT('Origin',(0.,0.,2.4));
#8679=CARTESIAN_POINT('',(-0.2,-2.44929359829471E-17,3.2));
#8680=CARTESIAN_POINT('Origin',(0.,0.,3.2));
#8681=CARTESIAN_POINT('',(-0.2,-2.44929359829471E-17,2.4));
#8682=CARTESIAN_POINT('',(-0.2,-2.44929359829471E-17,2.4));
#8683=CARTESIAN_POINT('Origin',(0.,0.,2.4));
#8684=CARTESIAN_POINT('Origin',(0.,0.,2.4));
#8685=CARTESIAN_POINT('',(-0.6,-7.34788079488412E-17,3.2));
#8686=CARTESIAN_POINT('Origin',(0.,0.,3.2));
#8687=CARTESIAN_POINT('',(-0.6,-7.34788079488412E-17,2.4));
#8688=CARTESIAN_POINT('',(-0.6,-7.34788079488412E-17,2.4));
#8689=CARTESIAN_POINT('Origin',(0.,0.,2.4));
#8690=CARTESIAN_POINT('Origin',(0.,0.,3.2));
#8691=CARTESIAN_POINT('Origin',(0.,0.,2.4));
#10224=UNCERTAINTY_MEASURE_WITH_UNIT(LENGTH_MEASURE(0.001),#10267,
'DISTANCE_ACCURACY_VALUE',
'Maximum model space distance between geometric entities at asserted c
onnectivities');
#10241=UNCERTAINTY_MEASURE_WITH_UNIT(LENGTH_MEASURE(0.001),#10267,
'DISTANCE_ACCURACY_VALUE',
'Maximum model space distance between geometric entities at asserted c
onnectivities');
#10249=(
GEOMETRIC_REPRESENTATION_CONTEXT(3)
GLOBAL_UNCERTAINTY_ASSIGNED_CONTEXT((#10224))
GLOBAL_UNIT_ASSIGNED_CONTEXT((#10267,#10269,#10270))
REPRESENTATION_CONTEXT('','3D')
);
#10266=(
GEOMETRIC_REPRESENTATION_CONTEXT(3)
GLOBAL_UNCERTAINTY_ASSIGNED_CONTEXT((#10241))
GLOBAL_UNIT_ASSIGNED_CONTEXT((#10267,#10269,#10270))
REPRESENTATION_CONTEXT('','3D')
);
#10267=(
LENGTH_UNIT()
NAMED_UNIT(*)
SI_UNIT(.CENTI.,.METRE.)
);
#10269=(
NAMED_UNIT(*)
PLANE_ANGLE_UNIT()
SI_UNIT($,.RADIAN.)
);
#10270=(
NAMED_UNIT(*)
SI_UNIT($,.STERADIAN.)
SOLID_ANGLE_UNIT()
);
#10278=SHAPE_DEFINITION_REPRESENTATION(#10302,#10361);
#10302=PRODUCT_DEFINITION_SHAPE('',$,#10386);
#10361=SHAPE_REPRESENTATION('',(#5222),#10249);
#10378=PRODUCT_DEFINITION_CONTEXT('part definition',#10452,'design');
#10386=PRODUCT_DEFINITION('Valve seat','Valve seat',#10410,
#10378);
#10410=PRODUCT_DEFINITION_FORMATION('',$,#10461);
#10452=APPLICATION_CONTEXT(
'Core Data for Automotive Mechanical Design Process');
#10453=PRODUCT_CONTEXT('part definition',#10452,'mechanical');
#10461=PRODUCT('Valve seat','Valve seat','Valve seat',(#10453));
#10555=COLOUR_RGB('Off White',0.89,0.88,0.83);
#10556=FILL_AREA_STYLE_COLOUR('',#10555);
#10557=FILL_AREA_STYLE('',(#10556));
#10558=SURFACE_STYLE_FILL_AREA(#10557);
#10559=SURFACE_SIDE_STYLE('',(#10558));
#10560=SURFACE_STYLE_USAGE(.BOTH.,#10559);
#10561=PRESENTATION_STYLE_ASSIGNMENT((#10560));
ENDSEC;
END-ISO-10303-21;
